ISO-10303-21;
HEADER;
/* Generated by software containing ST-Developer
 * from STEP Tools, Inc. (www.steptools.com) 
 */

FILE_DESCRIPTION(
/* description */ ('Bearing friction torque test rig'),
/* implementation_level */ '2;1');

FILE_NAME(
/* name */ 'Outer ring (1).step',
/* time_stamp */ '2026-10-28T03:24:04-07:00',
/* author */ (''),
/* organization */ (''),
/* preprocessor_version */ 'ST-DEVELOPER v20.2',
/* originating_system */ 'Autodesk Translation Framework v15.17.0.0',
/* authorisation */ '');

FILE_SCHEMA (('AUTOMOTIVE_DESIGN { 1 0 10303 214 3 1 1 }'));
ENDSEC;

DATA;
#10=MECHANICAL_DESIGN_GEOMETRIC_PRESENTATION_REPRESENTATION('',(#568),#14822);
#428=TOROIDAL_SURFACE('',#8772,1.675,0.412776);
#438=CONICAL_SURFACE('',#8783,2.3,0.785398163397449);
#439=CONICAL_SURFACE('',#8787,2.3,0.785398163397449);
#483=SHAPE_REPRESENTATION_RELATIONSHIP('SRR','None',#15024,#522);
#522=ADVANCED_BREP_SHAPE_REPRESENTATION('',(#621),#14804);
#568=STYLED_ITEM('',(#15284),#621);
#621=MANIFOLD_SOLID_BREP('Body1',#7685);
#825=FACE_BOUND('',#2021,.T.);
#826=FACE_BOUND('',#2026,.T.);
#1020=PLANE('',#8780);
#1021=PLANE('',#8789);
#1392=FACE_OUTER_BOUND('',#2018,.T.);
#1393=FACE_OUTER_BOUND('',#2019,.T.);
#1394=FACE_OUTER_BOUND('',#2020,.T.);
#1395=FACE_OUTER_BOUND('',#2022,.T.);
#1396=FACE_OUTER_BOUND('',#2023,.T.);
#1397=FACE_OUTER_BOUND('',#2024,.T.);
#1398=FACE_OUTER_BOUND('',#2025,.T.);
#1399=FACE_OUTER_BOUND('',#2027,.T.);
#2018=EDGE_LOOP('',(#6434,#6435,#6436,#6437,#6438,#6439));
#2019=EDGE_LOOP('',(#6440,#6441,#6442,#6443,#6444));
#2020=EDGE_LOOP('',(#6445));
#2021=EDGE_LOOP('',(#6446));
#2022=EDGE_LOOP('',(#6447,#6448,#6449,#6450));
#2023=EDGE_LOOP('',(#6451,#6452,#6453,#6454));
#2024=EDGE_LOOP('',(#6455,#6456,#6457,#6458));
#2025=EDGE_LOOP('',(#6459));
#2026=EDGE_LOOP('',(#6460));
#2027=EDGE_LOOP('',(#6461,#6462,#6463,#6464,#6465));
#2543=LINE('',#13368,#2987);
#2544=LINE('',#13377,#2988);
#2545=LINE('',#13381,#2989);
#2546=LINE('',#13385,#2990);
#2547=LINE('',#13388,#2991);
#2987=VECTOR('',#10766,1.71469);
#2988=VECTOR('',#10777,2.3);
#2989=VECTOR('',#10782,2.35);
#2990=VECTOR('',#10787,2.3);
#2991=VECTOR('',#10792,1.71469);
#3406=CIRCLE('',#8773,1.71469);
#3407=CIRCLE('',#8774,1.71469);
#3408=CIRCLE('',#8775,0.412776);
#3409=CIRCLE('',#8776,1.71469);
#3410=CIRCLE('',#8777,1.71469);
#3411=CIRCLE('',#8779,1.71469);
#3412=CIRCLE('',#8781,2.25);
#3413=CIRCLE('',#8782,1.71469);
#3414=CIRCLE('',#8784,2.35);
#3415=CIRCLE('',#8786,2.35);
#3416=CIRCLE('',#8788,2.25);
#3988=VERTEX_POINT('',#13356);
#3989=VERTEX_POINT('',#13357);
#3990=VERTEX_POINT('',#13360);
#3991=VERTEX_POINT('',#13362);
#3992=VERTEX_POINT('',#13366);
#3993=VERTEX_POINT('',#13370);
#3994=VERTEX_POINT('',#13372);
#3995=VERTEX_POINT('',#13375);
#3996=VERTEX_POINT('',#13379);
#3997=VERTEX_POINT('',#13383);
#4843=EDGE_CURVE('',#3988,#3989,#3406,.T.);
#4844=EDGE_CURVE('',#3989,#3988,#3407,.T.);
#4845=EDGE_CURVE('',#3989,#3990,#3408,.T.);
#4846=EDGE_CURVE('',#3991,#3990,#3409,.T.);
#4847=EDGE_CURVE('',#3990,#3991,#3410,.T.);
#4848=EDGE_CURVE('',#3992,#3992,#3411,.T.);
#4849=EDGE_CURVE('',#3992,#3991,#2543,.T.);
#4850=EDGE_CURVE('',#3993,#3993,#3412,.T.);
#4851=EDGE_CURVE('',#3994,#3994,#3413,.T.);
#4852=EDGE_CURVE('',#3995,#3995,#3414,.T.);
#4853=EDGE_CURVE('',#3995,#3993,#2544,.T.);
#4854=EDGE_CURVE('',#3996,#3996,#3415,.T.);
#4855=EDGE_CURVE('',#3996,#3995,#2545,.T.);
#4856=EDGE_CURVE('',#3997,#3997,#3416,.T.);
#4857=EDGE_CURVE('',#3997,#3996,#2546,.T.);
#4858=EDGE_CURVE('',#3988,#3994,#2547,.T.);
#6434=ORIENTED_EDGE('',*,*,#4843,.F.);
#6435=ORIENTED_EDGE('',*,*,#4844,.F.);
#6436=ORIENTED_EDGE('',*,*,#4845,.T.);
#6437=ORIENTED_EDGE('',*,*,#4846,.F.);
#6438=ORIENTED_EDGE('',*,*,#4847,.F.);
#6439=ORIENTED_EDGE('',*,*,#4845,.F.);
#6440=ORIENTED_EDGE('',*,*,#4848,.T.);
#6441=ORIENTED_EDGE('',*,*,#4849,.T.);
#6442=ORIENTED_EDGE('',*,*,#4846,.T.);
#6443=ORIENTED_EDGE('',*,*,#4847,.T.);
#6444=ORIENTED_EDGE('',*,*,#4849,.F.);
#6445=ORIENTED_EDGE('',*,*,#4850,.F.);
#6446=ORIENTED_EDGE('',*,*,#4851,.T.);
#6447=ORIENTED_EDGE('',*,*,#4852,.F.);
#6448=ORIENTED_EDGE('',*,*,#4853,.T.);
#6449=ORIENTED_EDGE('',*,*,#4850,.T.);
#6450=ORIENTED_EDGE('',*,*,#4853,.F.);
#6451=ORIENTED_EDGE('',*,*,#4854,.F.);
#6452=ORIENTED_EDGE('',*,*,#4855,.T.);
#6453=ORIENTED_EDGE('',*,*,#4852,.T.);
#6454=ORIENTED_EDGE('',*,*,#4855,.F.);
#6455=ORIENTED_EDGE('',*,*,#4856,.F.);
#6456=ORIENTED_EDGE('',*,*,#4857,.T.);
#6457=ORIENTED_EDGE('',*,*,#4854,.T.);
#6458=ORIENTED_EDGE('',*,*,#4857,.F.);
#6459=ORIENTED_EDGE('',*,*,#4856,.T.);
#6460=ORIENTED_EDGE('',*,*,#4848,.F.);
#6461=ORIENTED_EDGE('',*,*,#4843,.T.);
#6462=ORIENTED_EDGE('',*,*,#4844,.T.);
#6463=ORIENTED_EDGE('',*,*,#4858,.T.);
#6464=ORIENTED_EDGE('',*,*,#4851,.F.);
#6465=ORIENTED_EDGE('',*,*,#4858,.F.);
#7165=CYLINDRICAL_SURFACE('',#8778,1.71469);
#7166=CYLINDRICAL_SURFACE('',#8785,2.35);
#7167=CYLINDRICAL_SURFACE('',#8790,1.71469);
#7503=ADVANCED_FACE('',(#1392),#428,.F.);
#7504=ADVANCED_FACE('',(#1393),#7165,.F.);
#7505=ADVANCED_FACE('',(#1394,#825),#1020,.T.);
#7506=ADVANCED_FACE('',(#1395),#438,.T.);
#7507=ADVANCED_FACE('',(#1396),#7166,.T.);
#7508=ADVANCED_FACE('',(#1397),#439,.T.);
#7509=ADVANCED_FACE('',(#1398,#826),#1021,.T.);
#7510=ADVANCED_FACE('',(#1399),#7167,.F.);
#7685=CLOSED_SHELL('',(#7503,#7504,#7505,#7506,#7507,#7508,#7509,#7510));
#8771=AXIS2_PLACEMENT_3D('',#13354,#10748,#10749);
#8772=AXIS2_PLACEMENT_3D('',#13355,#10750,#10751);
#8773=AXIS2_PLACEMENT_3D('',#13358,#10752,#10753);
#8774=AXIS2_PLACEMENT_3D('',#13359,#10754,#10755);
#8775=AXIS2_PLACEMENT_3D('',#13361,#10756,#10757);
#8776=AXIS2_PLACEMENT_3D('',#13363,#10758,#10759);
#8777=AXIS2_PLACEMENT_3D('',#13364,#10760,#10761);
#8778=AXIS2_PLACEMENT_3D('',#13365,#10762,#10763);
#8779=AXIS2_PLACEMENT_3D('',#13367,#10764,#10765);
#8780=AXIS2_PLACEMENT_3D('',#13369,#10767,#10768);
#8781=AXIS2_PLACEMENT_3D('',#13371,#10769,#10770);
#8782=AXIS2_PLACEMENT_3D('',#13373,#10771,#10772);
#8783=AXIS2_PLACEMENT_3D('',#13374,#10773,#10774);
#8784=AXIS2_PLACEMENT_3D('',#13376,#10775,#10776);
#8785=AXIS2_PLACEMENT_3D('',#13378,#10778,#10779);
#8786=AXIS2_PLACEMENT_3D('',#13380,#10780,#10781);
#8787=AXIS2_PLACEMENT_3D('',#13382,#10783,#10784);
#8788=AXIS2_PLACEMENT_3D('',#13384,#10785,#10786);
#8789=AXIS2_PLACEMENT_3D('',#13386,#10788,#10789);
#8790=AXIS2_PLACEMENT_3D('',#13387,#10790,#10791);
#10748=DIRECTION('axis',(0.,0.,1.));
#10749=DIRECTION('refdir',(1.,0.,0.));
#10750=DIRECTION('center_axis',(0.,-1.,0.));
#10751=DIRECTION('ref_axis',(0.,0.,-1.));
#10752=DIRECTION('center_axis',(0.,-1.,0.));
#10753=DIRECTION('ref_axis',(1.,0.,0.));
#10754=DIRECTION('center_axis',(0.,-1.,0.));
#10755=DIRECTION('ref_axis',(1.,0.,0.));
#10756=DIRECTION('center_axis',(1.,0.,1.22464679914735E-16));
#10757=DIRECTION('ref_axis',(-1.22464679914735E-16,0.,1.));
#10758=DIRECTION('center_axis',(0.,1.,0.));
#10759=DIRECTION('ref_axis',(1.,0.,0.));
#10760=DIRECTION('center_axis',(0.,1.,0.));
#10761=DIRECTION('ref_axis',(1.,0.,0.));
#10762=DIRECTION('center_axis',(0.,-1.,0.));
#10763=DIRECTION('ref_axis',(1.,0.,0.));
#10764=DIRECTION('center_axis',(0.,-1.,0.));
#10765=DIRECTION('ref_axis',(1.,0.,0.));
#10766=DIRECTION('',(0.,1.,0.));
#10767=DIRECTION('center_axis',(0.,1.,0.));
#10768=DIRECTION('ref_axis',(0.,0.,1.));
#10769=DIRECTION('center_axis',(0.,-1.,0.));
#10770=DIRECTION('ref_axis',(1.,0.,0.));
#10771=DIRECTION('center_axis',(0.,-1.,0.));
#10772=DIRECTION('ref_axis',(1.,0.,0.));
#10773=DIRECTION('center_axis',(0.,-1.,0.));
#10774=DIRECTION('ref_axis',(1.,0.,0.));
#10775=DIRECTION('center_axis',(0.,-1.,0.));
#10776=DIRECTION('ref_axis',(1.,0.,0.));
#10777=DIRECTION('',(0.707106781186548,0.707106781186547,8.65956056235494E-17));
#10778=DIRECTION('center_axis',(0.,-1.,0.));
#10779=DIRECTION('ref_axis',(1.,0.,0.));
#10780=DIRECTION('center_axis',(0.,-1.,0.));
#10781=DIRECTION('ref_axis',(1.,0.,0.));
#10782=DIRECTION('',(0.,1.,0.));
#10783=DIRECTION('center_axis',(0.,1.,0.));
#10784=DIRECTION('ref_axis',(1.,0.,0.));
#10785=DIRECTION('center_axis',(0.,-1.,0.));
#10786=DIRECTION('ref_axis',(1.,0.,0.));
#10787=DIRECTION('',(-0.707106781186548,0.707106781186547,-8.65956056235494E-17));
#10788=DIRECTION('center_axis',(0.,-1.,0.));
#10789=DIRECTION('ref_axis',(0.,0.,-1.));
#10790=DIRECTION('center_axis',(0.,-1.,0.));
#10791=DIRECTION('ref_axis',(1.,0.,0.));
#10792=DIRECTION('',(0.,1.,0.));
#13354=CARTESIAN_POINT('',(0.,0.,0.));
#13355=CARTESIAN_POINT('Origin',(0.,0.,0.));
#13356=CARTESIAN_POINT('',(-1.71469,0.410863395882378,-2.09988962002998E-16));
#13357=CARTESIAN_POINT('',(-2.09988962002998E-16,0.410863395882378,1.71469));
#13358=CARTESIAN_POINT('Origin',(0.,0.410863395882378,0.));
#13359=CARTESIAN_POINT('Origin',(0.,0.410863395882378,0.));
#13360=CARTESIAN_POINT('',(-2.09988962002998E-16,-0.410863395882378,1.71469));
#13361=CARTESIAN_POINT('Origin',(-2.05128338857182E-16,0.,1.675));
#13362=CARTESIAN_POINT('',(-1.71469,-0.410863395882378,2.09988962002998E-16));
#13363=CARTESIAN_POINT('Origin',(0.,-0.410863395882378,0.));
#13364=CARTESIAN_POINT('Origin',(0.,-0.410863395882378,0.));
#13365=CARTESIAN_POINT('Origin',(0.,0.,0.));
#13366=CARTESIAN_POINT('',(-1.71469,-0.7,-2.09988962002998E-16));
#13367=CARTESIAN_POINT('Origin',(0.,-0.7,0.));
#13368=CARTESIAN_POINT('',(-1.71469,0.,-2.09988962002998E-16));
#13369=CARTESIAN_POINT('Origin',(2.25,0.7,0.));
#13370=CARTESIAN_POINT('',(-2.25,0.7,-2.75545529808154E-16));
#13371=CARTESIAN_POINT('Origin',(0.,0.7,0.));
#13372=CARTESIAN_POINT('',(-1.71469,0.7,-2.09988962002998E-16));
#13373=CARTESIAN_POINT('Origin',(0.,0.7,0.));
#13374=CARTESIAN_POINT('Origin',(0.,0.65,0.));
#13375=CARTESIAN_POINT('',(-2.35,0.6,-2.87791997799628E-16));
#13376=CARTESIAN_POINT('Origin',(0.,0.6,0.));
#13377=CARTESIAN_POINT('',(-2.3,0.65,-2.81668763803891E-16));
#13378=CARTESIAN_POINT('Origin',(0.,0.,0.));
#13379=CARTESIAN_POINT('',(-2.35,-0.6,-2.87791997799628E-16));
#13380=CARTESIAN_POINT('Origin',(0.,-0.6,0.));
#13381=CARTESIAN_POINT('',(-2.35,0.,-2.87791997799628E-16));
#13382=CARTESIAN_POINT('Origin',(0.,-0.65,0.));
#13383=CARTESIAN_POINT('',(-2.25,-0.7,-2.75545529808154E-16));
#13384=CARTESIAN_POINT('Origin',(0.,-0.7,0.));
#13385=CARTESIAN_POINT('',(-2.3,-0.65,-2.81668763803891E-16));
#13386=CARTESIAN_POINT('Origin',(1.71469,-0.7,0.));
#13387=CARTESIAN_POINT('Origin',(0.,0.,0.));
#13388=CARTESIAN_POINT('',(-1.71469,0.,-2.09988962002998E-16));
#14759=UNCERTAINTY_MEASURE_WITH_UNIT(LENGTH_MEASURE(0.001),#14823,
'DISTANCE_ACCURACY_VALUE',
'Maximum model space distance between geometric entities at asserted c
onnectivities');
#14777=UNCERTAINTY_MEASURE_WITH_UNIT(LENGTH_MEASURE(0.001),#14823,
'DISTANCE_ACCURACY_VALUE',
'Maximum model space distance between geometric entities at asserted c
onnectivities');
#14804=(
GEOMETRIC_REPRESENTATION_CONTEXT(3)
GLOBAL_UNCERTAINTY_ASSIGNED_CONTEXT((#14759))
GLOBAL_UNIT_ASSIGNED_CONTEXT((#14823,#14825,#14826))
REPRESENTATION_CONTEXT('','3D')
);
#14822=(
GEOMETRIC_REPRESENTATION_CONTEXT(3)
GLOBAL_UNCERTAINTY_ASSIGNED_CONTEXT((#14777))
GLOBAL_UNIT_ASSIGNED_CONTEXT((#14823,#14825,#14826))
REPRESENTATION_CONTEXT('','3D')
);
#14823=(
LENGTH_UNIT()
NAMED_UNIT(*)
SI_UNIT(.CENTI.,.METRE.)
);
#14825=(
NAMED_UNIT(*)
PLANE_ANGLE_UNIT()
SI_UNIT($,.RADIAN.)
);
#14826=(
NAMED_UNIT(*)
SI_UNIT($,.STERADIAN.)
SOLID_ANGLE_UNIT()
);
#14853=SHAPE_DEFINITION_REPRESENTATION(#14902,#15024);
#14902=PRODUCT_DEFINITION_SHAPE('',$,#15069);
#15024=SHAPE_REPRESENTATION('',(#8771),#14804);
#15042=PRODUCT_DEFINITION_CONTEXT('part definition',#15176,'design');
#15069=PRODUCT_DEFINITION('Outer ring (1)','Outer ring (1)',#15113,#15042);
#15113=PRODUCT_DEFINITION_FORMATION('',$,#15204);
#15176=APPLICATION_CONTEXT(
'Core Data for Automotive Mechanical Design Process');
#15177=PRODUCT_CONTEXT('part definition',#15176,'mechanical');
#15204=PRODUCT('Outer ring (1)','Outer ring (1)','Outer ring (1)',(#15177));
#15278=COLOUR_RGB('Grey',0.48,0.52,0.57);
#15279=FILL_AREA_STYLE_COLOUR('',#15278);
#15280=FILL_AREA_STYLE('',(#15279));
#15281=SURFACE_STYLE_FILL_AREA(#15280);
#15282=SURFACE_SIDE_STYLE('',(#15281));
#15283=SURFACE_STYLE_USAGE(.BOTH.,#15282);
#15284=PRESENTATION_STYLE_ASSIGNMENT((#15283));
ENDSEC;
END-ISO-10303-21;
